ISO-10303-21;
HEADER;
/* Generated by software containing ST-Developer
 * from STEP Tools, Inc. (www.steptools.com) 
 */

FILE_DESCRIPTION(
/* description */ ('Cam-and-follower valve demonstrator'),
/* implementation_level */ '2;1');

FILE_NAME(
/* name */ 'M4x10 Cap Screw.step',
/* time_stamp */ '2026-10-28T03:25:17-07:00',
/* author */ (''),
/* organization */ (''),
/* preprocessor_version */ 'ST-DEVELOPER v20.2',
/* originating_system */ 'Autodesk Translation Framework v15.17.0.0',
/* authorisation */ '');

FILE_SCHEMA (('AUTOMOTIVE_DESIGN { 1 0 10303 214 3 1 1 }'));
ENDSEC;

DATA;
#10=MECHANICAL_DESIGN_GEOMETRIC_PRESENTATION_REPRESENTATION('',(#439),#12896);
#12=ORIENTED_CLOSED_SHELL('',*,#6207,.F.);
#15=BREP_WITH_VOIDS('Body1',#6208,(#12));
#315=CONICAL_SURFACE('',#7133,0.325,0.785398163397448);
#316=CONICAL_SURFACE('',#7137,0.335,0.785398163397448);
#317=CONICAL_SURFACE('',#7141,0.21,0.463647609000806);
#360=SHAPE_REPRESENTATION_RELATIONSHIP('SRR','None',#13078,#396);
#396=ADVANCED_BREP_SHAPE_REPRESENTATION('',(#15),#12878);
#439=STYLED_ITEM('',(#13337),#15);
#625=FACE_BOUND('',#1844,.T.);
#890=CIRCLE('',#7130,0.1954);
#891=CIRCLE('',#7132,0.3);
#892=CIRCLE('',#7134,0.35);
#893=CIRCLE('',#7136,0.35);
#894=CIRCLE('',#7138,0.32);
#895=CIRCLE('',#7140,0.22);
#896=CIRCLE('',#7142,0.1954);
#1060=CYLINDRICAL_SURFACE('',#7135,0.35);
#1061=CYLINDRICAL_SURFACE('',#7143,0.1954);
#1332=FACE_OUTER_BOUND('',#1830,.T.);
#1333=FACE_OUTER_BOUND('',#1831,.T.);
#1334=FACE_OUTER_BOUND('',#1832,.T.);
#1335=FACE_OUTER_BOUND('',#1833,.T.);
#1336=FACE_OUTER_BOUND('',#1834,.T.);
#1337=FACE_OUTER_BOUND('',#1835,.T.);
#1338=FACE_OUTER_BOUND('',#1836,.T.);
#1339=FACE_OUTER_BOUND('',#1837,.T.);
#1340=FACE_OUTER_BOUND('',#1838,.T.);
#1341=FACE_OUTER_BOUND('',#1839,.T.);
#1342=FACE_OUTER_BOUND('',#1840,.T.);
#1343=FACE_OUTER_BOUND('',#1841,.T.);
#1344=FACE_OUTER_BOUND('',#1842,.T.);
#1345=FACE_OUTER_BOUND('',#1843,.T.);
#1346=FACE_OUTER_BOUND('',#1845,.T.);
#1347=FACE_OUTER_BOUND('',#1846,.T.);
#1830=EDGE_LOOP('',(#5113,#5114,#5115,#5116));
#1831=EDGE_LOOP('',(#5117,#5118,#5119,#5120));
#1832=EDGE_LOOP('',(#5121,#5122,#5123,#5124));
#1833=EDGE_LOOP('',(#5125,#5126,#5127,#5128));
#1834=EDGE_LOOP('',(#5129,#5130,#5131,#5132));
#1835=EDGE_LOOP('',(#5133,#5134,#5135,#5136));
#1836=EDGE_LOOP('',(#5137,#5138,#5139,#5140,#5141,#5142));
#1837=EDGE_LOOP('',(#5143,#5144,#5145,#5146,#5147,#5148));
#1838=EDGE_LOOP('',(#5149));
#1839=EDGE_LOOP('',(#5150));
#1840=EDGE_LOOP('',(#5151,#5152,#5153,#5154));
#1841=EDGE_LOOP('',(#5155,#5156,#5157,#5158));
#1842=EDGE_LOOP('',(#5159,#5160,#5161,#5162));
#1843=EDGE_LOOP('',(#5163));
#1844=EDGE_LOOP('',(#5164));
#1845=EDGE_LOOP('',(#5165,#5166,#5167,#5168));
#1846=EDGE_LOOP('',(#5169,#5170,#5171,#5172));
#2258=LINE('',#12203,#2680);
#2259=LINE('',#12205,#2681);
#2260=LINE('',#12207,#2682);
#2261=LINE('',#12208,#2683);
#2262=LINE('',#12211,#2684);
#2263=LINE('',#12213,#2685);
#2264=LINE('',#12214,#2686);
#2265=LINE('',#12217,#2687);
#2266=LINE('',#12219,#2688);
#2267=LINE('',#12220,#2689);
#2268=LINE('',#12223,#2690);
#2269=LINE('',#12225,#2691);
#2270=LINE('',#12226,#2692);
#2271=LINE('',#12229,#2693);
#2272=LINE('',#12231,#2694);
#2273=LINE('',#12232,#2695);
#2274=LINE('',#12234,#2696);
#2275=LINE('',#12235,#2697);
#2276=LINE('',#12247,#2698);
#2277=LINE('',#12251,#2699);
#2278=LINE('',#12255,#2700);
#2279=LINE('',#12262,#2701);
#2280=LINE('',#12264,#2702);
#2680=VECTOR('',#8677,1.);
#2681=VECTOR('',#8678,1.);
#2682=VECTOR('',#8679,1.);
#2683=VECTOR('',#8680,1.);
#2684=VECTOR('',#8683,1.);
#2685=VECTOR('',#8684,1.);
#2686=VECTOR('',#8685,1.);
#2687=VECTOR('',#8688,1.);
#2688=VECTOR('',#8689,1.);
#2689=VECTOR('',#8690,1.);
#2690=VECTOR('',#8693,1.);
#2691=VECTOR('',#8694,1.);
#2692=VECTOR('',#8695,1.);
#2693=VECTOR('',#8698,1.);
#2694=VECTOR('',#8699,1.);
#2695=VECTOR('',#8700,1.);
#2696=VECTOR('',#8703,1.);
#2697=VECTOR('',#8704,1.);
#2698=VECTOR('',#8721,0.325);
#2699=VECTOR('',#8726,0.35);
#2700=VECTOR('',#8731,0.335);
#2701=VECTOR('',#8740,0.21);
#2702=VECTOR('',#8743,0.2);
#3185=VERTEX_POINT('',#12201);
#3186=VERTEX_POINT('',#12202);
#3187=VERTEX_POINT('',#12204);
#3188=VERTEX_POINT('',#12206);
#3189=VERTEX_POINT('',#12210);
#3190=VERTEX_POINT('',#12212);
#3191=VERTEX_POINT('',#12216);
#3192=VERTEX_POINT('',#12218);
#3193=VERTEX_POINT('',#12222);
#3194=VERTEX_POINT('',#12224);
#3195=VERTEX_POINT('',#12228);
#3196=VERTEX_POINT('',#12230);
#3197=VERTEX_POINT('',#12239);
#3198=VERTEX_POINT('',#12242);
#3199=VERTEX_POINT('',#12245);
#3200=VERTEX_POINT('',#12249);
#3201=VERTEX_POINT('',#12253);
#3202=VERTEX_POINT('',#12257);
#3203=VERTEX_POINT('',#12260);
#3853=EDGE_CURVE('',#3185,#3186,#2258,.T.);
#3854=EDGE_CURVE('',#3186,#3187,#2259,.T.);
#3855=EDGE_CURVE('',#3187,#3188,#2260,.T.);
#3856=EDGE_CURVE('',#3185,#3188,#2261,.T.);
#3857=EDGE_CURVE('',#3186,#3189,#2262,.T.);
#3858=EDGE_CURVE('',#3189,#3190,#2263,.T.);
#3859=EDGE_CURVE('',#3190,#3187,#2264,.T.);
#3860=EDGE_CURVE('',#3189,#3191,#2265,.T.);
#3861=EDGE_CURVE('',#3191,#3192,#2266,.T.);
#3862=EDGE_CURVE('',#3192,#3190,#2267,.T.);
#3863=EDGE_CURVE('',#3191,#3193,#2268,.T.);
#3864=EDGE_CURVE('',#3193,#3194,#2269,.T.);
#3865=EDGE_CURVE('',#3194,#3192,#2270,.T.);
#3866=EDGE_CURVE('',#3193,#3195,#2271,.T.);
#3867=EDGE_CURVE('',#3195,#3196,#2272,.T.);
#3868=EDGE_CURVE('',#3196,#3194,#2273,.T.);
#3869=EDGE_CURVE('',#3195,#3185,#2274,.T.);
#3870=EDGE_CURVE('',#3188,#3196,#2275,.T.);
#3871=EDGE_CURVE('',#3197,#3197,#890,.T.);
#3872=EDGE_CURVE('',#3198,#3198,#891,.T.);
#3873=EDGE_CURVE('',#3199,#3199,#892,.T.);
#3874=EDGE_CURVE('',#3199,#3198,#2276,.T.);
#3875=EDGE_CURVE('',#3200,#3200,#893,.T.);
#3876=EDGE_CURVE('',#3200,#3199,#2277,.T.);
#3877=EDGE_CURVE('',#3201,#3201,#894,.T.);
#3878=EDGE_CURVE('',#3201,#3200,#2278,.T.);
#3879=EDGE_CURVE('',#3202,#3202,#895,.T.);
#3880=EDGE_CURVE('',#3203,#3203,#896,.F.);
#3881=EDGE_CURVE('',#3203,#3202,#2279,.T.);
#3882=EDGE_CURVE('',#3197,#3203,#2280,.T.);
#5113=ORIENTED_EDGE('',*,*,#3853,.T.);
#5114=ORIENTED_EDGE('',*,*,#3854,.T.);
#5115=ORIENTED_EDGE('',*,*,#3855,.T.);
#5116=ORIENTED_EDGE('',*,*,#3856,.F.);
#5117=ORIENTED_EDGE('',*,*,#3857,.T.);
#5118=ORIENTED_EDGE('',*,*,#3858,.T.);
#5119=ORIENTED_EDGE('',*,*,#3859,.T.);
#5120=ORIENTED_EDGE('',*,*,#3854,.F.);
#5121=ORIENTED_EDGE('',*,*,#3860,.T.);
#5122=ORIENTED_EDGE('',*,*,#3861,.T.);
#5123=ORIENTED_EDGE('',*,*,#3862,.T.);
#5124=ORIENTED_EDGE('',*,*,#3858,.F.);
#5125=ORIENTED_EDGE('',*,*,#3863,.T.);
#5126=ORIENTED_EDGE('',*,*,#3864,.T.);
#5127=ORIENTED_EDGE('',*,*,#3865,.T.);
#5128=ORIENTED_EDGE('',*,*,#3861,.F.);
#5129=ORIENTED_EDGE('',*,*,#3866,.T.);
#5130=ORIENTED_EDGE('',*,*,#3867,.T.);
#5131=ORIENTED_EDGE('',*,*,#3868,.T.);
#5132=ORIENTED_EDGE('',*,*,#3864,.F.);
#5133=ORIENTED_EDGE('',*,*,#3869,.T.);
#5134=ORIENTED_EDGE('',*,*,#3856,.T.);
#5135=ORIENTED_EDGE('',*,*,#3870,.T.);
#5136=ORIENTED_EDGE('',*,*,#3867,.F.);
#5137=ORIENTED_EDGE('',*,*,#3869,.F.);
#5138=ORIENTED_EDGE('',*,*,#3866,.F.);
#5139=ORIENTED_EDGE('',*,*,#3863,.F.);
#5140=ORIENTED_EDGE('',*,*,#3860,.F.);
#5141=ORIENTED_EDGE('',*,*,#3857,.F.);
#5142=ORIENTED_EDGE('',*,*,#3853,.F.);
#5143=ORIENTED_EDGE('',*,*,#3870,.F.);
#5144=ORIENTED_EDGE('',*,*,#3855,.F.);
#5145=ORIENTED_EDGE('',*,*,#3859,.F.);
#5146=ORIENTED_EDGE('',*,*,#3862,.F.);
#5147=ORIENTED_EDGE('',*,*,#3865,.F.);
#5148=ORIENTED_EDGE('',*,*,#3868,.F.);
#5149=ORIENTED_EDGE('',*,*,#3871,.F.);
#5150=ORIENTED_EDGE('',*,*,#3872,.F.);
#5151=ORIENTED_EDGE('',*,*,#3873,.F.);
#5152=ORIENTED_EDGE('',*,*,#3874,.T.);
#5153=ORIENTED_EDGE('',*,*,#3872,.T.);
#5154=ORIENTED_EDGE('',*,*,#3874,.F.);
#5155=ORIENTED_EDGE('',*,*,#3875,.F.);
#5156=ORIENTED_EDGE('',*,*,#3876,.T.);
#5157=ORIENTED_EDGE('',*,*,#3873,.T.);
#5158=ORIENTED_EDGE('',*,*,#3876,.F.);
#5159=ORIENTED_EDGE('',*,*,#3877,.F.);
#5160=ORIENTED_EDGE('',*,*,#3878,.T.);
#5161=ORIENTED_EDGE('',*,*,#3875,.T.);
#5162=ORIENTED_EDGE('',*,*,#3878,.F.);
#5163=ORIENTED_EDGE('',*,*,#3877,.T.);
#5164=ORIENTED_EDGE('',*,*,#3879,.F.);
#5165=ORIENTED_EDGE('',*,*,#3880,.F.);
#5166=ORIENTED_EDGE('',*,*,#3881,.T.);
#5167=ORIENTED_EDGE('',*,*,#3879,.T.);
#5168=ORIENTED_EDGE('',*,*,#3881,.F.);
#5169=ORIENTED_EDGE('',*,*,#3871,.T.);
#5170=ORIENTED_EDGE('',*,*,#3882,.T.);
#5171=ORIENTED_EDGE('',*,*,#3880,.T.);
#5172=ORIENTED_EDGE('',*,*,#3882,.F.);
#5722=PLANE('',#7121);
#5723=PLANE('',#7122);
#5724=PLANE('',#7123);
#5725=PLANE('',#7124);
#5726=PLANE('',#7125);
#5727=PLANE('',#7126);
#5728=PLANE('',#7127);
#5729=PLANE('',#7128);
#5730=PLANE('',#7129);
#5731=PLANE('',#7131);
#5732=PLANE('',#7139);
#6048=ADVANCED_FACE('',(#1332),#5722,.F.);
#6049=ADVANCED_FACE('',(#1333),#5723,.F.);
#6050=ADVANCED_FACE('',(#1334),#5724,.F.);
#6051=ADVANCED_FACE('',(#1335),#5725,.F.);
#6052=ADVANCED_FACE('',(#1336),#5726,.F.);
#6053=ADVANCED_FACE('',(#1337),#5727,.F.);
#6054=ADVANCED_FACE('',(#1338),#5728,.F.);
#6055=ADVANCED_FACE('',(#1339),#5729,.F.);
#6056=ADVANCED_FACE('',(#1340),#5730,.F.);
#6057=ADVANCED_FACE('',(#1341),#5731,.T.);
#6058=ADVANCED_FACE('',(#1342),#315,.T.);
#6059=ADVANCED_FACE('',(#1343),#1060,.T.);
#6060=ADVANCED_FACE('',(#1344),#316,.T.);
#6061=ADVANCED_FACE('',(#1345,#625),#5732,.T.);
#6062=ADVANCED_FACE('',(#1346),#317,.T.);
#6063=ADVANCED_FACE('',(#1347),#1061,.T.);
#6207=CLOSED_SHELL('',(#6048,#6049,#6050,#6051,#6052,#6053,#6054,#6055));
#6208=CLOSED_SHELL('',(#6056,#6057,#6058,#6059,#6060,#6061,#6062,#6063));
#7120=AXIS2_PLACEMENT_3D('',#12199,#8673,#8674);
#7121=AXIS2_PLACEMENT_3D('',#12200,#8675,#8676);
#7122=AXIS2_PLACEMENT_3D('',#12209,#8681,#8682);
#7123=AXIS2_PLACEMENT_3D('',#12215,#8686,#8687);
#7124=AXIS2_PLACEMENT_3D('',#12221,#8691,#8692);
#7125=AXIS2_PLACEMENT_3D('',#12227,#8696,#8697);
#7126=AXIS2_PLACEMENT_3D('',#12233,#8701,#8702);
#7127=AXIS2_PLACEMENT_3D('',#12236,#8705,#8706);
#7128=AXIS2_PLACEMENT_3D('',#12237,#8707,#8708);
#7129=AXIS2_PLACEMENT_3D('',#12238,#8709,#8710);
#7130=AXIS2_PLACEMENT_3D('',#12240,#8711,#8712);
#7131=AXIS2_PLACEMENT_3D('',#12241,#8713,#8714);
#7132=AXIS2_PLACEMENT_3D('',#12243,#8715,#8716);
#7133=AXIS2_PLACEMENT_3D('',#12244,#8717,#8718);
#7134=AXIS2_PLACEMENT_3D('',#12246,#8719,#8720);
#7135=AXIS2_PLACEMENT_3D('',#12248,#8722,#8723);
#7136=AXIS2_PLACEMENT_3D('',#12250,#8724,#8725);
#7137=AXIS2_PLACEMENT_3D('',#12252,#8727,#8728);
#7138=AXIS2_PLACEMENT_3D('',#12254,#8729,#8730);
#7139=AXIS2_PLACEMENT_3D('',#12256,#8732,#8733);
#7140=AXIS2_PLACEMENT_3D('',#12258,#8734,#8735);
#7141=AXIS2_PLACEMENT_3D('',#12259,#8736,#8737);
#7142=AXIS2_PLACEMENT_3D('',#12261,#8738,#8739);
#7143=AXIS2_PLACEMENT_3D('',#12263,#8741,#8742);
#8673=DIRECTION('axis',(0.,0.,1.));
#8674=DIRECTION('refdir',(1.,0.,0.));
#8675=DIRECTION('center_axis',(0.866025403784439,0.,-0.5));
#8676=DIRECTION('ref_axis',(0.5,0.,0.866025403784439));
#8677=DIRECTION('',(-0.5,0.,-0.866025403784439));
#8678=DIRECTION('',(0.,-1.,0.));
#8679=DIRECTION('',(0.5,0.,0.866025403784439));
#8680=DIRECTION('',(0.,-1.,0.));
#8681=DIRECTION('center_axis',(1.60246890531964E-16,0.,-1.));
#8682=DIRECTION('ref_axis',(1.,0.,1.60246890531964E-16));
#8683=DIRECTION('',(-1.,0.,-1.60246890531964E-16));
#8684=DIRECTION('',(0.,-1.,0.));
#8685=DIRECTION('',(1.,0.,1.60246890531964E-16));
#8686=DIRECTION('center_axis',(-0.866025403784439,0.,-0.5));
#8687=DIRECTION('ref_axis',(0.5,0.,-0.866025403784439));
#8688=DIRECTION('',(-0.5,0.,0.866025403784439));
#8689=DIRECTION('',(0.,-1.,0.));
#8690=DIRECTION('',(0.5,0.,-0.866025403784439));
#8691=DIRECTION('center_axis',(-0.866025403784439,0.,0.5));
#8692=DIRECTION('ref_axis',(-0.5,0.,-0.866025403784439));
#8693=DIRECTION('',(0.5,0.,0.866025403784439));
#8694=DIRECTION('',(0.,-1.,0.));
#8695=DIRECTION('',(-0.5,0.,-0.866025403784439));
#8696=DIRECTION('center_axis',(-1.60246890531964E-16,0.,1.));
#8697=DIRECTION('ref_axis',(-1.,0.,-1.60246890531964E-16));
#8698=DIRECTION('',(1.,0.,1.60246890531964E-16));
#8699=DIRECTION('',(0.,-1.,0.));
#8700=DIRECTION('',(-1.,0.,-1.60246890531964E-16));
#8701=DIRECTION('center_axis',(0.866025403784439,0.,0.5));
#8702=DIRECTION('ref_axis',(-0.5,0.,0.866025403784439));
#8703=DIRECTION('',(0.5,0.,-0.866025403784439));
#8704=DIRECTION('',(-0.5,0.,0.866025403784439));
#8705=DIRECTION('center_axis',(0.,1.,0.));
#8706=DIRECTION('ref_axis',(1.,0.,0.));
#8707=DIRECTION('center_axis',(0.,-1.,0.));
#8708=DIRECTION('ref_axis',(0.,0.,-1.));
#8709=DIRECTION('center_axis',(0.,1.,0.));
#8710=DIRECTION('ref_axis',(1.,0.,0.));
#8711=DIRECTION('center_axis',(0.,1.,0.));
#8712=DIRECTION('ref_axis',(1.,0.,0.));
#8713=DIRECTION('center_axis',(0.,1.,0.));
#8714=DIRECTION('ref_axis',(0.,0.,1.));
#8715=DIRECTION('center_axis',(0.,-1.,0.));
#8716=DIRECTION('ref_axis',(1.,0.,0.));
#8717=DIRECTION('center_axis',(0.,-1.,0.));
#8718=DIRECTION('ref_axis',(1.,0.,0.));
#8719=DIRECTION('center_axis',(0.,-1.,0.));
#8720=DIRECTION('ref_axis',(1.,0.,0.));
#8721=DIRECTION('',(0.707106781186547,0.707106781186548,8.65956056235493E-17));
#8722=DIRECTION('center_axis',(0.,-1.,0.));
#8723=DIRECTION('ref_axis',(1.,0.,0.));
#8724=DIRECTION('center_axis',(0.,-1.,0.));
#8725=DIRECTION('ref_axis',(1.,0.,0.));
#8726=DIRECTION('',(0.,1.,0.));
#8727=DIRECTION('center_axis',(0.,1.,0.));
#8728=DIRECTION('ref_axis',(1.,0.,0.));
#8729=DIRECTION('center_axis',(0.,-1.,0.));
#8730=DIRECTION('ref_axis',(1.,0.,0.));
#8731=DIRECTION('',(-0.707106781186547,0.707106781186548,-8.65956056235493E-17));
#8732=DIRECTION('center_axis',(0.,-1.,0.));
#8733=DIRECTION('ref_axis',(0.,0.,-1.));
#8734=DIRECTION('center_axis',(0.,-1.,0.));
#8735=DIRECTION('ref_axis',(1.,0.,0.));
#8736=DIRECTION('center_axis',(0.,1.,0.));
#8737=DIRECTION('ref_axis',(1.,0.,0.));
#8738=DIRECTION('center_axis',(0.,1.,0.));
#8739=DIRECTION('ref_axis',(1.,0.,0.));
#8740=DIRECTION('',(-0.447213595499958,0.894427190999916,-5.47678698264203E-17));
#8741=DIRECTION('center_axis',(0.,-1.,0.));
#8742=DIRECTION('ref_axis',(1.,0.,0.));
#8743=DIRECTION('',(0.,1.,0.));
#12199=CARTESIAN_POINT('',(0.,0.,0.));
#12200=CARTESIAN_POINT('Origin',(0.0866025403784439,-0.4,-0.15));
#12201=CARTESIAN_POINT('',(0.173205080756888,-0.4,0.));
#12202=CARTESIAN_POINT('',(0.0866025403784439,-0.4,-0.15));
#12203=CARTESIAN_POINT('',(0.173205080756888,-0.4,0.));
#12204=CARTESIAN_POINT('',(0.0866025403784439,-0.64,-0.15));
#12205=CARTESIAN_POINT('',(0.0866025403784439,-0.4,-0.15));
#12206=CARTESIAN_POINT('',(0.173205080756888,-0.64,0.));
#12207=CARTESIAN_POINT('',(0.173205080756888,-0.64,0.));
#12208=CARTESIAN_POINT('',(0.173205080756888,-0.4,0.));
#12209=CARTESIAN_POINT('Origin',(-0.0866025403784438,-0.4,-0.15));
#12210=CARTESIAN_POINT('',(-0.0866025403784438,-0.4,-0.15));
#12211=CARTESIAN_POINT('',(0.0866025403784439,-0.4,-0.15));
#12212=CARTESIAN_POINT('',(-0.0866025403784438,-0.64,-0.15));
#12213=CARTESIAN_POINT('',(-0.0866025403784438,-0.4,-0.15));
#12214=CARTESIAN_POINT('',(0.0866025403784439,-0.64,-0.15));
#12215=CARTESIAN_POINT('Origin',(-0.173205080756888,-0.4,-2.77555756156289E-17));
#12216=CARTESIAN_POINT('',(-0.173205080756888,-0.4,-2.12115047744981E-17));
#12217=CARTESIAN_POINT('',(-0.0866025403784438,-0.4,-0.15));
#12218=CARTESIAN_POINT('',(-0.173205080756888,-0.64,-2.77555756156289E-17));
#12219=CARTESIAN_POINT('',(-0.173205080756888,-0.4,-2.12115047744981E-17));
#12220=CARTESIAN_POINT('',(-0.0866025403784438,-0.64,-0.15));
#12221=CARTESIAN_POINT('Origin',(-0.0866025403784439,-0.4,0.15));
#12222=CARTESIAN_POINT('',(-0.0866025403784439,-0.4,0.15));
#12223=CARTESIAN_POINT('',(-0.173205080756888,-0.4,-2.12115047744981E-17));
#12224=CARTESIAN_POINT('',(-0.0866025403784439,-0.64,0.15));
#12225=CARTESIAN_POINT('',(-0.0866025403784439,-0.4,0.15));
#12226=CARTESIAN_POINT('',(-0.173205080756888,-0.64,-2.12115047744981E-17));
#12227=CARTESIAN_POINT('Origin',(0.0866025403784439,-0.4,0.15));
#12228=CARTESIAN_POINT('',(0.0866025403784439,-0.4,0.15));
#12229=CARTESIAN_POINT('',(-0.0866025403784439,-0.4,0.15));
#12230=CARTESIAN_POINT('',(0.0866025403784439,-0.64,0.15));
#12231=CARTESIAN_POINT('',(0.0866025403784439,-0.4,0.15));
#12232=CARTESIAN_POINT('',(-0.0866025403784439,-0.64,0.15));
#12233=CARTESIAN_POINT('Origin',(0.173205080756888,-0.4,0.));
#12234=CARTESIAN_POINT('',(0.0866025403784439,-0.4,0.15));
#12235=CARTESIAN_POINT('',(0.0866025403784439,-0.64,0.15));
#12236=CARTESIAN_POINT('Origin',(0.,-0.4,-2.77555756156289E-17));
#12237=CARTESIAN_POINT('Origin',(0.,-0.64,-2.77555756156289E-17));
#12238=CARTESIAN_POINT('Origin',(0.,-1.,0.));
#12239=CARTESIAN_POINT('',(-0.1954,-1.,2.39295984553393E-17));
#12240=CARTESIAN_POINT('Origin',(0.,-1.,0.));
#12241=CARTESIAN_POINT('Origin',(0.3,0.4,0.));
#12242=CARTESIAN_POINT('',(-0.3,0.4,-3.67394039744206E-17));
#12243=CARTESIAN_POINT('Origin',(0.,0.4,0.));
#12244=CARTESIAN_POINT('Origin',(0.,0.375,0.));
#12245=CARTESIAN_POINT('',(-0.35,0.35,-4.28626379701573E-17));
#12246=CARTESIAN_POINT('Origin',(0.,0.35,0.));
#12247=CARTESIAN_POINT('',(-0.325,0.375,-3.9801020972289E-17));
#12248=CARTESIAN_POINT('Origin',(0.,0.19,0.));
#12249=CARTESIAN_POINT('',(-0.35,0.03,-4.28626379701574E-17));
#12250=CARTESIAN_POINT('Origin',(0.,0.03,0.));
#12251=CARTESIAN_POINT('',(-0.35,0.19,-4.28626379701574E-17));
#12252=CARTESIAN_POINT('Origin',(0.,0.0149999999999999,0.));
#12253=CARTESIAN_POINT('',(-0.32,-3.29597460435593E-17,-3.91886975727153E-17));
#12254=CARTESIAN_POINT('Origin',(0.,0.,0.));
#12255=CARTESIAN_POINT('',(-0.335,0.0149999999999999,-4.10256677714363E-17));
#12256=CARTESIAN_POINT('Origin',(0.22,0.,0.));
#12257=CARTESIAN_POINT('',(-0.22,-6.93889390390723E-18,-2.69422295812418E-17));
#12258=CARTESIAN_POINT('Origin',(0.,0.,0.));
#12259=CARTESIAN_POINT('Origin',(0.,-0.02,0.));
#12260=CARTESIAN_POINT('',(-0.1954,-0.0492,2.39295984553393E-17));
#12261=CARTESIAN_POINT('Origin',(0.,-0.0492,0.));
#12262=CARTESIAN_POINT('',(-0.21,-0.02,-2.57175827820944E-17));
#12263=CARTESIAN_POINT('Origin',(0.,-0.8,0.));
#12264=CARTESIAN_POINT('',(-0.1954,-0.8,-2.39295984553393E-17));
#12835=UNCERTAINTY_MEASURE_WITH_UNIT(LENGTH_MEASURE(0.001),#12897,
'DISTANCE_ACCURACY_VALUE',
'Maximum model space distance between geometric entities at asserted c
onnectivities');
#12853=UNCERTAINTY_MEASURE_WITH_UNIT(LENGTH_MEASURE(0.001),#12897,
'DISTANCE_ACCURACY_VALUE',
'Maximum model space distance between geometric entities at asserted c
onnectivities');
#12878=(
GEOMETRIC_REPRESENTATION_CONTEXT(3)
GLOBAL_UNCERTAINTY_ASSIGNED_CONTEXT((#12835))
GLOBAL_UNIT_ASSIGNED_CONTEXT((#12897,#12899,#12900))
REPRESENTATION_CONTEXT('','3D')
);
#12896=(
GEOMETRIC_REPRESENTATION_CONTEXT(3)
GLOBAL_UNCERTAINTY_ASSIGNED_CONTEXT((#12853))
GLOBAL_UNIT_ASSIGNED_CONTEXT((#12897,#12899,#12900))
REPRESENTATION_CONTEXT('','3D')
);
#12897=(
LENGTH_UNIT()
NAMED_UNIT(*)
SI_UNIT(.CENTI.,.METRE.)
);
#12899=(
NAMED_UNIT(*)
PLANE_ANGLE_UNIT()
SI_UNIT($,.RADIAN.)
);
#12900=(
NAMED_UNIT(*)
SI_UNIT($,.STERADIAN.)
SOLID_ANGLE_UNIT()
);
#12925=SHAPE_DEFINITION_REPRESENTATION(#12974,#13078);
#12974=PRODUCT_DEFINITION_SHAPE('',$,#13121);
#13078=SHAPE_REPRESENTATION('',(#7120),#12878);
#13096=PRODUCT_DEFINITION_CONTEXT('part definition',#13224,'design');
#13121=PRODUCT_DEFINITION('M4x10 Cap Screw','M4x10 Cap Screw',#13163,#13096);
#13163=PRODUCT_DEFINITION_FORMATION('',$,#13250);
#13224=APPLICATION_CONTEXT(
'Core Data for Automotive Mechanical Design Process');
#13225=PRODUCT_CONTEXT('part definition',#13224,'mechanical');
#13250=PRODUCT('M4x10 Cap Screw','M4x10 Cap Screw','M4x10 Cap Screw',(#13225));
#13331=COLOUR_RGB('Black',0.12,0.14,0.17);
#13332=FILL_AREA_STYLE_COLOUR('',#13331);
#13333=FILL_AREA_STYLE('',(#13332));
#13334=SURFACE_STYLE_FILL_AREA(#13333);
#13335=SURFACE_SIDE_STYLE('',(#13334));
#13336=SURFACE_STYLE_USAGE(.BOTH.,#13335);
#13337=PRESENTATION_STYLE_ASSIGNMENT((#13336));
ENDSEC;
END-ISO-10303-21;
